ISO-10303-21;
HEADER;
FILE_DESCRIPTION (('STEP AP214'),
    '1' );
FILE_NAME ('pulley bushing.step',
    '2026-10-12T23:53:07',
    ( '' ),
    ( '' ),
    'SwSTEP 2.0',
    'SolidWorks 2024',
    '' );
FILE_SCHEMA (( 'AUTOMOTIVE_DESIGN' ));
ENDSEC;

DATA;
#150=CYLINDRICAL_SURFACE ( 'NONE', #28383, 0.1249999999999999584 ) ;
#734=ORIENTED_EDGE ( 'NONE', *, *, #40360, .T. ) ;
#805=CARTESIAN_POINT ( 'NONE',  ( 0.1399999999999994582, 1.942890293094021357E-17, 0.05000000000000000971 ) ) ;
#840=DIRECTION ( 'NONE',  ( 1.000000000000000000, 2.403560570595279103E-31, -1.725633230170969455E-31 ) ) ;
#1126=( CONVERSION_BASED_UNIT ( 'INCH', #10967 ) LENGTH_UNIT ( ) NAMED_UNIT ( #23398 ) );
#1145=ORIENTED_EDGE ( 'NONE', *, *, #12551, .T. ) ;
#1331=ORIENTED_EDGE ( 'NONE', *, *, #35960, .T. ) ;
#1632=AXIS2_PLACEMENT_3D ( 'NONE', #32854, #17232, #37557 ) ;
#1713=FACE_OUTER_BOUND ( 'NONE', #20602, .T. ) ;
#1791=ORIENTED_EDGE ( 'NONE', *, *, #14862, .F. ) ;
#1993=ORIENTED_EDGE ( 'NONE', *, *, #40360, .F. ) ;
#2152=ADVANCED_FACE ( 'NONE', ( #31571 ), #150, .T. ) ;
#2626=PRODUCT_DEFINITION ( 'UNKNOWN', '', #36468, #7610 ) ;
#2712=EDGE_CURVE ( 'NONE', #6499, #34235, #22814, .T. ) ;
#2931=ORIENTED_EDGE ( 'NONE', *, *, #3385, .F. ) ;
#2961=DIRECTION ( 'NONE',  ( 0.000000000000000000, 0.000000000000000000, 1.000000000000000000 ) ) ;
#3385=EDGE_CURVE ( 'NONE', #33435, #17597, #6238, .T. ) ;
#3879=CARTESIAN_POINT ( 'NONE',  ( 0.1399999999999994582, 0.000000000000000000, 0.000000000000000000 ) ) ;
#4045=CARTESIAN_POINT ( 'NONE',  ( 0.1399999999999994582, -1.330566893520349807E-17, -0.04999999999999998890 ) ) ;
#4116=EDGE_CURVE ( 'NONE', #39495, #24591, #14135, .T. ) ;
#4234=CARTESIAN_POINT ( 'NONE',  ( -0.1399999999999997358, 1.942890293094021357E-17, 0.05000000000000000971 ) ) ;
#4289=CYLINDRICAL_SURFACE ( 'NONE', #22418, 0.04999999999999998890 ) ;
#4380=ORIENTED_EDGE ( 'NONE', *, *, #32627, .F. ) ;
#4587=CARTESIAN_POINT ( 'NONE',  ( -0.1399999999999997358, 0.000000000000000000, 0.000000000000000000 ) ) ;
#4641=AXIS2_PLACEMENT_3D ( 'NONE', #3879, #840, #10280 ) ;
#4648=DIRECTION ( 'NONE',  ( -1.000000000000000000, -2.403560570595279103E-31, 1.725633230170969455E-31 ) ) ;
#4824=CIRCLE ( 'NONE', #22614, 0.04999999999999998890 ) ;
#5097=ORIENTED_EDGE ( 'NONE', *, *, #37671, .T. ) ;
#5467=CIRCLE ( 'NONE', #6795, 0.1249999999999999584 ) ;
#5656=DIRECTION ( 'NONE',  ( 0.000000000000000000, 3.885780586188049371E-16, 1.000000000000000000 ) ) ;
#5802=DIRECTION ( 'NONE',  ( 1.417484439069006026E-31, -3.885780586188048878E-16, -1.000000000000000000 ) ) ;
#5985=CARTESIAN_POINT ( 'NONE',  ( 0.1399999999999994582, -1.330566893520353813E-17, -0.05000000000000000971 ) ) ;
#6238=CIRCLE ( 'NONE', #25975, 0.1249999999999999584 ) ;
#6499=VERTEX_POINT ( 'NONE', #5985 ) ;
#6795=AXIS2_PLACEMENT_3D ( 'NONE', #34597, #21651, #31105 ) ;
#6936=DIRECTION ( 'NONE',  ( -1.000000000000000000, -2.403560570595279103E-31, 1.725633230170969455E-31 ) ) ;
#6968=CARTESIAN_POINT ( 'NONE',  ( 0.1399999999999994582, 0.000000000000000000, 0.000000000000000000 ) ) ;
#7610=PRODUCT_DEFINITION_CONTEXT ( 'detailed design', #21638, 'design' ) ;
#7660=( CONVERSION_BASED_UNIT ( 'INCH', #39331 ) LENGTH_UNIT ( ) NAMED_UNIT ( #22863 ) );
#8176=ADVANCED_FACE ( 'NONE', ( #38233 ), #4289, .F. ) ;
#8194=EDGE_CURVE ( 'NONE', #6499, #39495, #27658, .T. ) ;
#8315=DIRECTION ( 'NONE',  ( 1.000000000000000000, 0.000000000000000000, 0.000000000000000000 ) ) ;
#8837=AXIS2_PLACEMENT_3D ( 'NONE', #4587, #29509, #35467 ) ;
#8920=CARTESIAN_POINT ( 'NONE',  ( 0.000000000000000000, 0.000000000000000000, 0.000000000000000000 ) ) ;
#9588=CLOSED_SHELL ( 'NONE', ( #26324, #21348, #25064, #36128, #2152, #8176 ) ) ;
#10119=DIRECTION ( 'NONE',  ( 0.000000000000000000, -3.885780586188049371E-16, -1.000000000000000000 ) ) ;
#10123=ORIENTED_EDGE ( 'NONE', *, *, #13972, .T. ) ;
#10280=DIRECTION ( 'NONE',  ( 0.000000000000000000, -3.885780586188049371E-16, -1.000000000000000000 ) ) ;
#10578=FACE_OUTER_BOUND ( 'NONE', #24970, .T. ) ;
#10751=SHAPE_REPRESENTATION_RELATIONSHIP ( 'NONE' , 'NONE' ,  #31708, #24078 ) ;
#10967=LENGTH_MEASURE_WITH_UNIT ( LENGTH_MEASURE( 0.02539999999999999897 ), #38919 );
#11399=( GEOMETRIC_REPRESENTATION_CONTEXT ( 3 ) GLOBAL_UNCERTAINTY_ASSIGNED_CONTEXT ( ( #15737 ) ) GLOBAL_UNIT_ASSIGNED_CONTEXT ( ( #1126, #26195, #23112 ) ) REPRESENTATION_CONTEXT ( 'NONE', 'WORKASPACE' ) );
#11614=DIRECTION ( 'NONE',  ( 0.000000000000000000, -3.885780586188049371E-16, -1.000000000000000000 ) ) ;
#11820=ORIENTED_EDGE ( 'NONE', *, *, #13972, .F. ) ;
#11842=ORIENTED_EDGE ( 'NONE', *, *, #14862, .T. ) ;
#11976=CARTESIAN_POINT ( 'NONE',  ( 0.1399999999999994582, 0.000000000000000000, 0.000000000000000000 ) ) ;
#12033=ORIENTED_EDGE ( 'NONE', *, *, #12551, .F. ) ;
#12324=CARTESIAN_POINT ( 'NONE',  ( 0.1399999999999994582, 4.857225732735056783E-17, 0.1250000000000000000 ) ) ;
#12500=EDGE_LOOP ( 'NONE', ( #30613, #14124, #1145, #13099 ) ) ;
#12551=EDGE_CURVE ( 'NONE', #22278, #27442, #5467, .T. ) ;
#12564=DIRECTION ( 'NONE',  ( -1.000000000000000000, -2.403560570595279103E-31, 1.725633230170969455E-31 ) ) ;
#12869=DIRECTION ( 'NONE',  ( 0.000000000000000000, 3.885780586188049371E-16, 1.000000000000000000 ) ) ;
#13099=ORIENTED_EDGE ( 'NONE', *, *, #37671, .F. ) ;
#13202=APPLICATION_CONTEXT ( 'configuration controlled 3d designs of mechanical parts and assemblies' ) ;
#13972=EDGE_CURVE ( 'NONE', #27442, #22278, #37081, .T. ) ;
#14124=ORIENTED_EDGE ( 'NONE', *, *, #30515, .T. ) ;
#14135=LINE ( 'NONE', #23430, #19418 ) ;
#14300=EDGE_LOOP ( 'NONE', ( #14505, #2931, #5097, #10123 ) ) ;
#14383=PRODUCT ( 'pulley bushing', 'pulley bushing', '', ( #22719 ) ) ;
#14505=ORIENTED_EDGE ( 'NONE', *, *, #30515, .F. ) ;
#14661=DIRECTION ( 'NONE',  ( 1.000000000000000000, 2.403560570595280416E-31, 1.417484439069005150E-31 ) ) ;
#14862=EDGE_CURVE ( 'NONE', #39495, #6499, #39481, .T. ) ;
#15000=CARTESIAN_POINT ( 'NONE',  ( 0.1399999999999994582, -3.326417233800878524E-17, -0.1250000000000000000 ) ) ;
#15265=DIRECTION ( 'NONE',  ( 1.000000000000000000, 2.403560570595279103E-31, -1.725633230170969455E-31 ) ) ;
#15682=LINE ( 'NONE', #33800, #16069 ) ;
#15737=UNCERTAINTY_MEASURE_WITH_UNIT (LENGTH_MEASURE( 1.000000000000000082E-05 ), #1126, 'distance_accuracy_value', 'NONE');
#16069=VECTOR ( 'NONE', #30908, 39.37007874015748143 ) ;
#17232=DIRECTION ( 'NONE',  ( 1.000000000000000000, 2.403560570595279103E-31, -1.725633230170969455E-31 ) ) ;
#17597=VERTEX_POINT ( 'NONE', #15000 ) ;
#17710=DIRECTION ( 'NONE',  ( 0.000000000000000000, 3.885780586188049371E-16, 1.000000000000000000 ) ) ;
#17793=CARTESIAN_POINT ( 'NONE',  ( 0.1399999999999994582, 0.000000000000000000, 0.000000000000000000 ) ) ;
#18131=DIRECTION ( 'NONE',  ( -1.000000000000000000, -2.403560570595279103E-31, 1.725633230170969455E-31 ) ) ;
#18630=DIRECTION ( 'NONE',  ( -1.000000000000000000, -2.403560570595279103E-31, 1.725633230170969455E-31 ) ) ;
#18757=LINE ( 'NONE', #24732, #24047 ) ;
#19040=CARTESIAN_POINT ( 'NONE',  ( 0.1399999999999994582, 0.000000000000000000, 0.000000000000000000 ) ) ;
#19418=VECTOR ( 'NONE', #4648, 39.37007874015748143 ) ;
#19456=UNCERTAINTY_MEASURE_WITH_UNIT (LENGTH_MEASURE( 1.000000000000000082E-05 ), #7660, 'distance_accuracy_value', 'NONE');
#19541=DIRECTION ( 'NONE',  ( -1.000000000000000000, -2.403560570595279103E-31, 1.725633230170969455E-31 ) ) ;
#19889=AXIS2_PLACEMENT_3D ( 'NONE', #30781, #37352, #21340 ) ;
#20602=EDGE_LOOP ( 'NONE', ( #11842, #26833, #1993, #36887 ) ) ;
#20655=FACE_OUTER_BOUND ( 'NONE', #30945, .T. ) ;
#21221=CARTESIAN_POINT ( 'NONE',  ( 0.1399999999999994582, 0.000000000000000000, 0.000000000000000000 ) ) ;
#21259=PLANE ( 'NONE',  #27654 ) ;
#21304=CIRCLE ( 'NONE', #25929, 0.1249999999999999584 ) ;
#21340=DIRECTION ( 'NONE',  ( 0.000000000000000000, -3.885780586188049371E-16, -1.000000000000000000 ) ) ;
#21348=ADVANCED_FACE ( 'NONE', ( #30352 ), #27285, .T. ) ;
#21627=ORIENTED_EDGE ( 'NONE', *, *, #3385, .T. ) ;
#21638=APPLICATION_CONTEXT ( 'configuration controlled 3d designs of mechanical parts and assemblies' ) ;
#21651=DIRECTION ( 'NONE',  ( 1.000000000000000000, 2.403560570595279103E-31, -1.725633230170969455E-31 ) ) ;
#21720=DIRECTION ( 'NONE',  ( 1.000000000000000000, 2.403560570595279103E-31, -1.725633230170969455E-31 ) ) ;
#22154=CARTESIAN_POINT ( 'NONE',  ( 0.1399999999999994582, 0.000000000000000000, 0.000000000000000000 ) ) ;
#22158=CARTESIAN_POINT ( 'NONE',  ( -0.1399999999999997358, 4.857225732735056783E-17, 0.1250000000000000000 ) ) ;
#22278=VERTEX_POINT ( 'NONE', #29920 ) ;
#22418=AXIS2_PLACEMENT_3D ( 'NONE', #6968, #19541, #32072 ) ;
#22614=AXIS2_PLACEMENT_3D ( 'NONE', #29038, #27884, #10119 ) ;
#22719=PRODUCT_CONTEXT ( 'NONE', #13202, 'mechanical' ) ;
#22814=LINE ( 'NONE', #4045, #34466 ) ;
#22863=DIMENSIONAL_EXPONENTS ( 1.000000000000000000, 0.000000000000000000, 0.000000000000000000, 0.000000000000000000, 0.000000000000000000, 0.000000000000000000, 0.000000000000000000 ) ;
#22950=PLANE ( 'NONE',  #8837 ) ;
#23112=( NAMED_UNIT ( * ) SI_UNIT ( $, .STERADIAN. ) SOLID_ANGLE_UNIT ( ) );
#23398=DIMENSIONAL_EXPONENTS ( 1.000000000000000000, 0.000000000000000000, 0.000000000000000000, 0.000000000000000000, 0.000000000000000000, 0.000000000000000000, 0.000000000000000000 ) ;
#23430=CARTESIAN_POINT ( 'NONE',  ( 0.1399999999999994582, 1.942890293094024131E-17, 0.04999999999999998890 ) ) ;
#24001=DIRECTION ( 'NONE',  ( -1.000000000000000000, -2.403560570595279103E-31, 1.725633230170969455E-31 ) ) ;
#24047=VECTOR ( 'NONE', #12564, 39.37007874015748143 ) ;
#24078=ADVANCED_BREP_SHAPE_REPRESENTATION ( '', ( #32841, #27819 ), #30435 ) ;
#24591=VERTEX_POINT ( 'NONE', #4234 ) ;
#24732=CARTESIAN_POINT ( 'NONE',  ( 0.1399999999999994582, 4.857225732735059864E-17, 0.1249999999999999584 ) ) ;
#24970=EDGE_LOOP ( 'NONE', ( #11820, #12033 ) ) ;
#25064=ADVANCED_FACE ( 'NONE', ( #20655, #39963 ), #21259, .T. ) ;
#25374=EDGE_LOOP ( 'NONE', ( #734, #33075 ) ) ;
#25875=ORIENTED_EDGE ( 'NONE', *, *, #8194, .F. ) ;
#25929=AXIS2_PLACEMENT_3D ( 'NONE', #22154, #21720, #37962 ) ;
#25975=AXIS2_PLACEMENT_3D ( 'NONE', #40174, #27453, #11614 ) ;
#26195=( NAMED_UNIT ( * ) PLANE_ANGLE_UNIT ( ) SI_UNIT ( $, .RADIAN. ) );
#26324=ADVANCED_FACE ( 'NONE', ( #1713 ), #30075, .F. ) ;
#26833=ORIENTED_EDGE ( 'NONE', *, *, #2712, .T. ) ;
#26894=PRODUCT_DEFINITION_SHAPE ( 'NONE', 'NONE',  #2626 ) ;
#27285=CYLINDRICAL_SURFACE ( 'NONE', #31864, 0.1249999999999999584 ) ;
#27442=VERTEX_POINT ( 'NONE', #22158 ) ;
#27453=DIRECTION ( 'NONE',  ( 1.000000000000000000, 2.403560570595279103E-31, -1.725633230170969455E-31 ) ) ;
#27654=AXIS2_PLACEMENT_3D ( 'NONE', #39356, #14661, #5802 ) ;
#27658=CIRCLE ( 'NONE', #4641, 0.04999999999999998890 ) ;
#27797=CIRCLE ( 'NONE', #19889, 0.04999999999999998890 ) ;
#27819=AXIS2_PLACEMENT_3D ( 'NONE', #8920, #2961, #8315 ) ;
#27884=DIRECTION ( 'NONE',  ( 1.000000000000000000, 2.403560570595279103E-31, -1.725633230170969455E-31 ) ) ;
#28383=AXIS2_PLACEMENT_3D ( 'NONE', #19040, #18630, #12869 ) ;
#29036=ORIENTED_EDGE ( 'NONE', *, *, #8194, .T. ) ;
#29038=CARTESIAN_POINT ( 'NONE',  ( -0.1399999999999997358, 0.000000000000000000, 0.000000000000000000 ) ) ;
#29509=DIRECTION ( 'NONE',  ( 1.000000000000000000, 2.403560570595280416E-31, 1.417484439069005150E-31 ) ) ;
#29884=( LENGTH_UNIT ( ) NAMED_UNIT ( * ) SI_UNIT ( $, .METRE. ) );
#29920=CARTESIAN_POINT ( 'NONE',  ( -0.1399999999999997358, -3.326417233800878524E-17, -0.1250000000000000000 ) ) ;
#30075=CYLINDRICAL_SURFACE ( 'NONE', #38218, 0.04999999999999998890 ) ;
#30352=FACE_OUTER_BOUND ( 'NONE', #12500, .T. ) ;
#30435=( GEOMETRIC_REPRESENTATION_CONTEXT ( 3 ) GLOBAL_UNCERTAINTY_ASSIGNED_CONTEXT ( ( #19456 ) ) GLOBAL_UNIT_ASSIGNED_CONTEXT ( ( #7660, #32548, #38719 ) ) REPRESENTATION_CONTEXT ( 'NONE', 'WORKASPACE' ) );
#30515=EDGE_CURVE ( 'NONE', #17597, #22278, #15682, .T. ) ;
#30613=ORIENTED_EDGE ( 'NONE', *, *, #35960, .F. ) ;
#30781=CARTESIAN_POINT ( 'NONE',  ( -0.1399999999999997358, 0.000000000000000000, 0.000000000000000000 ) ) ;
#30908=DIRECTION ( 'NONE',  ( -1.000000000000000000, -2.403560570595279103E-31, 1.725633230170969455E-31 ) ) ;
#30945=EDGE_LOOP ( 'NONE', ( #21627, #1331 ) ) ;
#31105=DIRECTION ( 'NONE',  ( 0.000000000000000000, -3.885780586188049371E-16, -1.000000000000000000 ) ) ;
#31538=SHAPE_DEFINITION_REPRESENTATION ( #26894, #31708 ) ;
#31571=FACE_OUTER_BOUND ( 'NONE', #14300, .T. ) ;
#31700=CARTESIAN_POINT ( 'NONE',  ( -0.1399999999999997358, -1.330566893520353813E-17, -0.05000000000000000971 ) ) ;
#31708=SHAPE_REPRESENTATION ( 'pulley bushing', ( #27819 ), #30435 ) ;
#31864=AXIS2_PLACEMENT_3D ( 'NONE', #17793, #24001, #5656 ) ;
#32072=DIRECTION ( 'NONE',  ( 0.000000000000000000, 3.885780586188049371E-16, 1.000000000000000000 ) ) ;
#32548=( NAMED_UNIT ( * ) PLANE_ANGLE_UNIT ( ) SI_UNIT ( $, .RADIAN. ) );
#32627=EDGE_CURVE ( 'NONE', #34235, #24591, #4824, .T. ) ;
#32841=MANIFOLD_SOLID_BREP ( 'Extrude-Thin1', #9588 ) ;
#32854=CARTESIAN_POINT ( 'NONE',  ( -0.1399999999999997358, 0.000000000000000000, 0.000000000000000000 ) ) ;
#33075=ORIENTED_EDGE ( 'NONE', *, *, #32627, .T. ) ;
#33435=VERTEX_POINT ( 'NONE', #12324 ) ;
#33481=EDGE_LOOP ( 'NONE', ( #39349, #29036, #37806, #4380 ) ) ;
#33800=CARTESIAN_POINT ( 'NONE',  ( 0.1399999999999994582, -3.326417233800874210E-17, -0.1249999999999999584 ) ) ;
#34235=VERTEX_POINT ( 'NONE', #31700 ) ;
#34390=DIRECTION ( 'NONE',  ( 0.000000000000000000, -3.885780586188049371E-16, -1.000000000000000000 ) ) ;
#34466=VECTOR ( 'NONE', #6936, 39.37007874015748143 ) ;
#34597=CARTESIAN_POINT ( 'NONE',  ( -0.1399999999999997358, 0.000000000000000000, 0.000000000000000000 ) ) ;
#35467=DIRECTION ( 'NONE',  ( 1.417484439069006026E-31, -3.885780586188048878E-16, -1.000000000000000000 ) ) ;
#35960=EDGE_CURVE ( 'NONE', #17597, #33435, #21304, .T. ) ;
#36128=ADVANCED_FACE ( 'NONE', ( #10578, #38563 ), #22950, .F. ) ;
#36468=PRODUCT_DEFINITION_FORMATION_WITH_SPECIFIED_SOURCE ( 'ANY', '', #14383, .NOT_KNOWN. ) ;
#36844=AXIS2_PLACEMENT_3D ( 'NONE', #11976, #15265, #34390 ) ;
#36887=ORIENTED_EDGE ( 'NONE', *, *, #4116, .F. ) ;
#37081=CIRCLE ( 'NONE', #1632, 0.1249999999999999584 ) ;
#37352=DIRECTION ( 'NONE',  ( 1.000000000000000000, 2.403560570595279103E-31, -1.725633230170969455E-31 ) ) ;
#37431=EDGE_LOOP ( 'NONE', ( #1791, #25875 ) ) ;
#37557=DIRECTION ( 'NONE',  ( 0.000000000000000000, -3.885780586188049371E-16, -1.000000000000000000 ) ) ;
#37671=EDGE_CURVE ( 'NONE', #33435, #27442, #18757, .T. ) ;
#37806=ORIENTED_EDGE ( 'NONE', *, *, #4116, .T. ) ;
#37962=DIRECTION ( 'NONE',  ( 0.000000000000000000, -3.885780586188049371E-16, -1.000000000000000000 ) ) ;
#38218=AXIS2_PLACEMENT_3D ( 'NONE', #21221, #18131, #17710 ) ;
#38233=FACE_OUTER_BOUND ( 'NONE', #33481, .T. ) ;
#38563=FACE_BOUND ( 'NONE', #25374, .T. ) ;
#38719=( NAMED_UNIT ( * ) SI_UNIT ( $, .STERADIAN. ) SOLID_ANGLE_UNIT ( ) );
#38919=( LENGTH_UNIT ( ) NAMED_UNIT ( * ) SI_UNIT ( $, .METRE. ) );
#39331=LENGTH_MEASURE_WITH_UNIT ( LENGTH_MEASURE( 0.02539999999999999897 ), #29884 );
#39349=ORIENTED_EDGE ( 'NONE', *, *, #2712, .F. ) ;
#39356=CARTESIAN_POINT ( 'NONE',  ( 0.1399999999999994582, 0.000000000000000000, 0.000000000000000000 ) ) ;
#39481=CIRCLE ( 'NONE', #36844, 0.04999999999999998890 ) ;
#39495=VERTEX_POINT ( 'NONE', #805 ) ;
#39963=FACE_BOUND ( 'NONE', #37431, .T. ) ;
#40174=CARTESIAN_POINT ( 'NONE',  ( 0.1399999999999994582, 0.000000000000000000, 0.000000000000000000 ) ) ;
#40360=EDGE_CURVE ( 'NONE', #24591, #34235, #27797, .T. ) ;
#40702=COLOUR_RGB('Off White',0.89,0.88,0.83);
#40703=FILL_AREA_STYLE_COLOUR('',#40702);
#40704=FILL_AREA_STYLE('',(#40703));
#40705=SURFACE_STYLE_FILL_AREA(#40704);
#40706=SURFACE_SIDE_STYLE('',(#40705));
#40707=SURFACE_STYLE_USAGE(.BOTH.,#40706);
#40708=PRESENTATION_STYLE_ASSIGNMENT((#40707));
#40711=STYLED_ITEM('',(#40708),#32841);
#40721=MECHANICAL_DESIGN_GEOMETRIC_PRESENTATION_REPRESENTATION('',(#40711),#11399);
ENDSEC;
END-ISO-10303-21;
